ISO-10303-21;
HEADER;
/* Generated by software containing ST-Developer
 * from STEP Tools, Inc. (www.steptools.com) 
 */

FILE_DESCRIPTION(
/* description */ ('Manifold and mounting hardware'),
/* implementation_level */ '2;1');

FILE_NAME(
/* name */ '1_4-1_8 in port reducer (3).step',
/* time_stamp */ '2026-10-28T21:46:49-07:00',
/* author */ (''),
/* organization */ (''),
/* preprocessor_version */ 'ST-DEVELOPER v20.2',
/* originating_system */ 'Autodesk Translation Framework v15.17.0.0',
/* authorisation */ '');

FILE_SCHEMA (('AUTOMOTIVE_DESIGN { 1 0 10303 214 3 1 1 }'));
ENDSEC;

DATA;
#10=MECHANICAL_DESIGN_GEOMETRIC_PRESENTATION_REPRESENTATION('',(#151),#5638);
#123=SHAPE_REPRESENTATION_RELATIONSHIP('SRR','None',#5702,#137);
#137=ADVANCED_BREP_SHAPE_REPRESENTATION('',(#165),#5624);
#151=STYLED_ITEM('',(#5853),#165);
#165=MANIFOLD_SOLID_BREP('Body1',#3141);
#196=FACE_BOUND('',#573,.T.);
#197=FACE_BOUND('',#575,.T.);
#198=FACE_BOUND('',#583,.T.);
#199=FACE_BOUND('',#587,.T.);
#288=CYLINDRICAL_SURFACE('',#3397,0.515);
#289=CYLINDRICAL_SURFACE('',#3411,0.2);
#290=CYLINDRICAL_SURFACE('',#3413,0.685);
#367=FACE_OUTER_BOUND('',#571,.T.);
#368=FACE_OUTER_BOUND('',#572,.T.);
#369=FACE_OUTER_BOUND('',#574,.T.);
#370=FACE_OUTER_BOUND('',#576,.T.);
#371=FACE_OUTER_BOUND('',#577,.T.);
#372=FACE_OUTER_BOUND('',#578,.T.);
#373=FACE_OUTER_BOUND('',#579,.T.);
#374=FACE_OUTER_BOUND('',#580,.T.);
#375=FACE_OUTER_BOUND('',#581,.T.);
#376=FACE_OUTER_BOUND('',#582,.T.);
#377=FACE_OUTER_BOUND('',#584,.T.);
#378=FACE_OUTER_BOUND('',#585,.T.);
#379=FACE_OUTER_BOUND('',#586,.T.);
#571=EDGE_LOOP('',(#2226,#2227,#2228,#2229));
#572=EDGE_LOOP('',(#2230));
#573=EDGE_LOOP('',(#2231));
#574=EDGE_LOOP('',(#2232,#2233,#2234,#2235,#2236,#2237));
#575=EDGE_LOOP('',(#2238));
#576=EDGE_LOOP('',(#2239,#2240,#2241,#2242));
#577=EDGE_LOOP('',(#2243,#2244,#2245,#2246));
#578=EDGE_LOOP('',(#2247,#2248,#2249,#2250));
#579=EDGE_LOOP('',(#2251,#2252,#2253,#2254));
#580=EDGE_LOOP('',(#2255,#2256,#2257,#2258));
#581=EDGE_LOOP('',(#2259,#2260,#2261,#2262));
#582=EDGE_LOOP('',(#2263,#2264,#2265,#2266,#2267,#2268));
#583=EDGE_LOOP('',(#2269));
#584=EDGE_LOOP('',(#2270,#2271,#2272,#2273));
#585=EDGE_LOOP('',(#2274,#2275,#2276,#2277));
#586=EDGE_LOOP('',(#2278));
#587=EDGE_LOOP('',(#2279));
#809=CIRCLE('',#3398,0.515);
#810=CIRCLE('',#3399,0.515);
#811=CIRCLE('',#3401,0.2);
#812=CIRCLE('',#3403,0.685);
#813=CIRCLE('',#3412,0.2);
#814=CIRCLE('',#3414,0.685);
#936=LINE('',#4908,#1183);
#937=LINE('',#4916,#1184);
#938=LINE('',#4918,#1185);
#939=LINE('',#4920,#1186);
#940=LINE('',#4922,#1187);
#941=LINE('',#4924,#1188);
#942=LINE('',#4925,#1189);
#943=LINE('',#4930,#1190);
#944=LINE('',#4932,#1191);
#945=LINE('',#4933,#1192);
#946=LINE('',#4936,#1193);
#947=LINE('',#4937,#1194);
#948=LINE('',#4940,#1195);
#949=LINE('',#4941,#1196);
#950=LINE('',#4944,#1197);
#951=LINE('',#4945,#1198);
#952=LINE('',#4948,#1199);
#953=LINE('',#4949,#1200);
#954=LINE('',#4951,#1201);
#955=LINE('',#4955,#1202);
#956=LINE('',#4959,#1203);
#1183=VECTOR('',#3891,0.515);
#1184=VECTOR('',#3900,1.);
#1185=VECTOR('',#3901,1.);
#1186=VECTOR('',#3902,1.);
#1187=VECTOR('',#3903,1.);
#1188=VECTOR('',#3904,1.);
#1189=VECTOR('',#3905,1.);
#1190=VECTOR('',#3910,1.);
#1191=VECTOR('',#3911,1.);
#1192=VECTOR('',#3912,1.);
#1193=VECTOR('',#3915,1.);
#1194=VECTOR('',#3916,1.);
#1195=VECTOR('',#3919,1.);
#1196=VECTOR('',#3920,1.);
#1197=VECTOR('',#3923,1.);
#1198=VECTOR('',#3924,1.);
#1199=VECTOR('',#3927,1.);
#1200=VECTOR('',#3928,1.);
#1201=VECTOR('',#3931,1.);
#1202=VECTOR('',#3936,0.2);
#1203=VECTOR('',#3941,0.685);
#1451=VERTEX_POINT('',#4905);
#1452=VERTEX_POINT('',#4907);
#1453=VERTEX_POINT('',#4911);
#1454=VERTEX_POINT('',#4914);
#1455=VERTEX_POINT('',#4915);
#1456=VERTEX_POINT('',#4917);
#1457=VERTEX_POINT('',#4919);
#1458=VERTEX_POINT('',#4921);
#1459=VERTEX_POINT('',#4923);
#1460=VERTEX_POINT('',#4926);
#1461=VERTEX_POINT('',#4929);
#1462=VERTEX_POINT('',#4931);
#1463=VERTEX_POINT('',#4935);
#1464=VERTEX_POINT('',#4939);
#1465=VERTEX_POINT('',#4943);
#1466=VERTEX_POINT('',#4947);
#1467=VERTEX_POINT('',#4954);
#1468=VERTEX_POINT('',#4958);
#1742=EDGE_CURVE('',#1451,#1451,#809,.T.);
#1743=EDGE_CURVE('',#1451,#1452,#936,.T.);
#1744=EDGE_CURVE('',#1452,#1452,#810,.T.);
#1745=EDGE_CURVE('',#1453,#1453,#811,.T.);
#1746=EDGE_CURVE('',#1454,#1455,#937,.T.);
#1747=EDGE_CURVE('',#1456,#1454,#938,.T.);
#1748=EDGE_CURVE('',#1457,#1456,#939,.T.);
#1749=EDGE_CURVE('',#1458,#1457,#940,.T.);
#1750=EDGE_CURVE('',#1459,#1458,#941,.T.);
#1751=EDGE_CURVE('',#1455,#1459,#942,.T.);
#1752=EDGE_CURVE('',#1460,#1460,#812,.T.);
#1753=EDGE_CURVE('',#1454,#1461,#943,.T.);
#1754=EDGE_CURVE('',#1462,#1461,#944,.T.);
#1755=EDGE_CURVE('',#1456,#1462,#945,.T.);
#1756=EDGE_CURVE('',#1463,#1462,#946,.T.);
#1757=EDGE_CURVE('',#1457,#1463,#947,.T.);
#1758=EDGE_CURVE('',#1464,#1463,#948,.T.);
#1759=EDGE_CURVE('',#1458,#1464,#949,.T.);
#1760=EDGE_CURVE('',#1465,#1464,#950,.T.);
#1761=EDGE_CURVE('',#1459,#1465,#951,.T.);
#1762=EDGE_CURVE('',#1466,#1465,#952,.T.);
#1763=EDGE_CURVE('',#1455,#1466,#953,.T.);
#1764=EDGE_CURVE('',#1461,#1466,#954,.T.);
#1765=EDGE_CURVE('',#1453,#1467,#955,.T.);
#1766=EDGE_CURVE('',#1467,#1467,#813,.T.);
#1767=EDGE_CURVE('',#1460,#1468,#956,.T.);
#1768=EDGE_CURVE('',#1468,#1468,#814,.T.);
#2226=ORIENTED_EDGE('',*,*,#1742,.F.);
#2227=ORIENTED_EDGE('',*,*,#1743,.T.);
#2228=ORIENTED_EDGE('',*,*,#1744,.F.);
#2229=ORIENTED_EDGE('',*,*,#1743,.F.);
#2230=ORIENTED_EDGE('',*,*,#1742,.T.);
#2231=ORIENTED_EDGE('',*,*,#1745,.F.);
#2232=ORIENTED_EDGE('',*,*,#1746,.F.);
#2233=ORIENTED_EDGE('',*,*,#1747,.F.);
#2234=ORIENTED_EDGE('',*,*,#1748,.F.);
#2235=ORIENTED_EDGE('',*,*,#1749,.F.);
#2236=ORIENTED_EDGE('',*,*,#1750,.F.);
#2237=ORIENTED_EDGE('',*,*,#1751,.F.);
#2238=ORIENTED_EDGE('',*,*,#1752,.T.);
#2239=ORIENTED_EDGE('',*,*,#1747,.T.);
#2240=ORIENTED_EDGE('',*,*,#1753,.T.);
#2241=ORIENTED_EDGE('',*,*,#1754,.F.);
#2242=ORIENTED_EDGE('',*,*,#1755,.F.);
#2243=ORIENTED_EDGE('',*,*,#1748,.T.);
#2244=ORIENTED_EDGE('',*,*,#1755,.T.);
#2245=ORIENTED_EDGE('',*,*,#1756,.F.);
#2246=ORIENTED_EDGE('',*,*,#1757,.F.);
#2247=ORIENTED_EDGE('',*,*,#1749,.T.);
#2248=ORIENTED_EDGE('',*,*,#1757,.T.);
#2249=ORIENTED_EDGE('',*,*,#1758,.F.);
#2250=ORIENTED_EDGE('',*,*,#1759,.F.);
#2251=ORIENTED_EDGE('',*,*,#1750,.T.);
#2252=ORIENTED_EDGE('',*,*,#1759,.T.);
#2253=ORIENTED_EDGE('',*,*,#1760,.F.);
#2254=ORIENTED_EDGE('',*,*,#1761,.F.);
#2255=ORIENTED_EDGE('',*,*,#1751,.T.);
#2256=ORIENTED_EDGE('',*,*,#1761,.T.);
#2257=ORIENTED_EDGE('',*,*,#1762,.F.);
#2258=ORIENTED_EDGE('',*,*,#1763,.F.);
#2259=ORIENTED_EDGE('',*,*,#1746,.T.);
#2260=ORIENTED_EDGE('',*,*,#1763,.T.);
#2261=ORIENTED_EDGE('',*,*,#1764,.F.);
#2262=ORIENTED_EDGE('',*,*,#1753,.F.);
#2263=ORIENTED_EDGE('',*,*,#1764,.T.);
#2264=ORIENTED_EDGE('',*,*,#1762,.T.);
#2265=ORIENTED_EDGE('',*,*,#1760,.T.);
#2266=ORIENTED_EDGE('',*,*,#1758,.T.);
#2267=ORIENTED_EDGE('',*,*,#1756,.T.);
#2268=ORIENTED_EDGE('',*,*,#1754,.T.);
#2269=ORIENTED_EDGE('',*,*,#1744,.T.);
#2270=ORIENTED_EDGE('',*,*,#1745,.T.);
#2271=ORIENTED_EDGE('',*,*,#1765,.T.);
#2272=ORIENTED_EDGE('',*,*,#1766,.T.);
#2273=ORIENTED_EDGE('',*,*,#1765,.F.);
#2274=ORIENTED_EDGE('',*,*,#1752,.F.);
#2275=ORIENTED_EDGE('',*,*,#1767,.T.);
#2276=ORIENTED_EDGE('',*,*,#1768,.T.);
#2277=ORIENTED_EDGE('',*,*,#1767,.F.);
#2278=ORIENTED_EDGE('',*,*,#1768,.F.);
#2279=ORIENTED_EDGE('',*,*,#1766,.F.);
#2852=PLANE('',#3400);
#2853=PLANE('',#3402);
#2854=PLANE('',#3404);
#2855=PLANE('',#3405);
#2856=PLANE('',#3406);
#2857=PLANE('',#3407);
#2858=PLANE('',#3408);
#2859=PLANE('',#3409);
#2860=PLANE('',#3410);
#2861=PLANE('',#3415);
#2991=ADVANCED_FACE('',(#367),#288,.F.);
#2992=ADVANCED_FACE('',(#368,#196),#2852,.T.);
#2993=ADVANCED_FACE('',(#369,#197),#2853,.F.);
#2994=ADVANCED_FACE('',(#370),#2854,.T.);
#2995=ADVANCED_FACE('',(#371),#2855,.T.);
#2996=ADVANCED_FACE('',(#372),#2856,.T.);
#2997=ADVANCED_FACE('',(#373),#2857,.T.);
#2998=ADVANCED_FACE('',(#374),#2858,.T.);
#2999=ADVANCED_FACE('',(#375),#2859,.T.);
#3000=ADVANCED_FACE('',(#376,#198),#2860,.T.);
#3001=ADVANCED_FACE('',(#377),#289,.F.);
#3002=ADVANCED_FACE('',(#378),#290,.T.);
#3003=ADVANCED_FACE('',(#379,#199),#2861,.F.);
#3141=CLOSED_SHELL('',(#2991,#2992,#2993,#2994,#2995,#2996,#2997,#2998,
#2999,#3000,#3001,#3002,#3003));
#3396=AXIS2_PLACEMENT_3D('',#4903,#3885,#3886);
#3397=AXIS2_PLACEMENT_3D('',#4904,#3887,#3888);
#3398=AXIS2_PLACEMENT_3D('',#4906,#3889,#3890);
#3399=AXIS2_PLACEMENT_3D('',#4909,#3892,#3893);
#3400=AXIS2_PLACEMENT_3D('',#4910,#3894,#3895);
#3401=AXIS2_PLACEMENT_3D('',#4912,#3896,#3897);
#3402=AXIS2_PLACEMENT_3D('',#4913,#3898,#3899);
#3403=AXIS2_PLACEMENT_3D('',#4927,#3906,#3907);
#3404=AXIS2_PLACEMENT_3D('',#4928,#3908,#3909);
#3405=AXIS2_PLACEMENT_3D('',#4934,#3913,#3914);
#3406=AXIS2_PLACEMENT_3D('',#4938,#3917,#3918);
#3407=AXIS2_PLACEMENT_3D('',#4942,#3921,#3922);
#3408=AXIS2_PLACEMENT_3D('',#4946,#3925,#3926);
#3409=AXIS2_PLACEMENT_3D('',#4950,#3929,#3930);
#3410=AXIS2_PLACEMENT_3D('',#4952,#3932,#3933);
#3411=AXIS2_PLACEMENT_3D('',#4953,#3934,#3935);
#3412=AXIS2_PLACEMENT_3D('',#4956,#3937,#3938);
#3413=AXIS2_PLACEMENT_3D('',#4957,#3939,#3940);
#3414=AXIS2_PLACEMENT_3D('',#4960,#3942,#3943);
#3415=AXIS2_PLACEMENT_3D('',#4961,#3944,#3945);
#3885=DIRECTION('axis',(0.,0.,1.));
#3886=DIRECTION('refdir',(1.,0.,0.));
#3887=DIRECTION('center_axis',(0.,0.,1.));
#3888=DIRECTION('ref_axis',(1.,0.,0.));
#3889=DIRECTION('center_axis',(0.,0.,1.));
#3890=DIRECTION('ref_axis',(1.,0.,0.));
#3891=DIRECTION('',(0.,0.,1.));
#3892=DIRECTION('center_axis',(0.,0.,-1.));
#3893=DIRECTION('ref_axis',(1.,0.,0.));
#3894=DIRECTION('center_axis',(0.,0.,1.));
#3895=DIRECTION('ref_axis',(1.,0.,0.));
#3896=DIRECTION('center_axis',(0.,0.,1.));
#3897=DIRECTION('ref_axis',(1.,0.,0.));
#3898=DIRECTION('center_axis',(0.,0.,1.));
#3899=DIRECTION('ref_axis',(1.,0.,0.));
#3900=DIRECTION('',(0.5,0.866025403784438,0.));
#3901=DIRECTION('',(1.,-3.29650746237182E-16,0.));
#3902=DIRECTION('',(0.499999999999999,-0.866025403784439,0.));
#3903=DIRECTION('',(-0.5,-0.866025403784439,0.));
#3904=DIRECTION('',(-1.,0.,0.));
#3905=DIRECTION('',(-0.5,0.866025403784438,0.));
#3906=DIRECTION('center_axis',(0.,0.,1.));
#3907=DIRECTION('ref_axis',(1.,0.,0.));
#3908=DIRECTION('center_axis',(-3.29650746237182E-16,-1.,0.));
#3909=DIRECTION('ref_axis',(1.,-3.29650746237182E-16,0.));
#3910=DIRECTION('',(0.,0.,1.));
#3911=DIRECTION('',(1.,-3.29650746237182E-16,0.));
#3912=DIRECTION('',(0.,0.,1.));
#3913=DIRECTION('center_axis',(-0.866025403784439,-0.499999999999999,0.));
#3914=DIRECTION('ref_axis',(0.499999999999999,-0.866025403784439,0.));
#3915=DIRECTION('',(0.499999999999999,-0.866025403784439,0.));
#3916=DIRECTION('',(0.,0.,1.));
#3917=DIRECTION('center_axis',(-0.866025403784439,0.5,0.));
#3918=DIRECTION('ref_axis',(-0.5,-0.866025403784439,0.));
#3919=DIRECTION('',(-0.5,-0.866025403784439,0.));
#3920=DIRECTION('',(0.,0.,1.));
#3921=DIRECTION('center_axis',(0.,1.,0.));
#3922=DIRECTION('ref_axis',(-1.,0.,0.));
#3923=DIRECTION('',(-1.,0.,0.));
#3924=DIRECTION('',(0.,0.,1.));
#3925=DIRECTION('center_axis',(0.866025403784438,0.5,0.));
#3926=DIRECTION('ref_axis',(-0.5,0.866025403784438,0.));
#3927=DIRECTION('',(-0.5,0.866025403784438,0.));
#3928=DIRECTION('',(0.,0.,1.));
#3929=DIRECTION('center_axis',(0.866025403784438,-0.5,0.));
#3930=DIRECTION('ref_axis',(0.5,0.866025403784438,0.));
#3931=DIRECTION('',(0.5,0.866025403784438,0.));
#3932=DIRECTION('center_axis',(0.,0.,1.));
#3933=DIRECTION('ref_axis',(1.,0.,0.));
#3934=DIRECTION('center_axis',(0.,0.,1.));
#3935=DIRECTION('ref_axis',(1.,0.,0.));
#3936=DIRECTION('',(0.,0.,-1.));
#3937=DIRECTION('center_axis',(0.,0.,-1.));
#3938=DIRECTION('ref_axis',(1.,0.,0.));
#3939=DIRECTION('center_axis',(0.,0.,1.));
#3940=DIRECTION('ref_axis',(1.,0.,0.));
#3941=DIRECTION('',(0.,0.,-1.));
#3942=DIRECTION('center_axis',(0.,0.,1.));
#3943=DIRECTION('ref_axis',(1.,0.,0.));
#3944=DIRECTION('center_axis',(0.,0.,1.));
#3945=DIRECTION('ref_axis',(1.,0.,0.));
#4903=CARTESIAN_POINT('',(0.,0.,0.));
#4904=CARTESIAN_POINT('Origin',(-3.75,0.,4.85));
#4905=CARTESIAN_POINT('',(-4.265,-6.30693101560887E-17,4.85));
#4906=CARTESIAN_POINT('Origin',(-3.75,0.,4.85));
#4907=CARTESIAN_POINT('',(-4.265,6.30693101560887E-17,5.5));
#4908=CARTESIAN_POINT('',(-4.265,-6.30693101560887E-17,4.85));
#4909=CARTESIAN_POINT('Origin',(-3.75,0.,5.5));
#4910=CARTESIAN_POINT('Origin',(-3.75,0.,4.85));
#4911=CARTESIAN_POINT('',(-3.95,-2.44929359829471E-17,4.85));
#4912=CARTESIAN_POINT('Origin',(-3.75,0.,4.85));
#4913=CARTESIAN_POINT('Origin',(-3.75,0.,5.));
#4914=CARTESIAN_POINT('',(-3.24481851445908,-0.875,5.));
#4915=CARTESIAN_POINT('',(-2.73963702891815,0.,5.));
#4916=CARTESIAN_POINT('',(-3.24481851445908,-0.875,5.));
#4917=CARTESIAN_POINT('',(-4.25518148554092,-0.875,5.));
#4918=CARTESIAN_POINT('',(-4.25518148554092,-0.875,5.));
#4919=CARTESIAN_POINT('',(-4.76036297108184,1.23733777851239E-16,5.));
#4920=CARTESIAN_POINT('',(-4.76036297108184,1.23733777851239E-16,5.));
#4921=CARTESIAN_POINT('',(-4.25518148554092,0.875,5.));
#4922=CARTESIAN_POINT('',(-4.25518148554092,0.875,5.));
#4923=CARTESIAN_POINT('',(-3.24481851445908,0.875,5.));
#4924=CARTESIAN_POINT('',(-3.24481851445908,0.875,5.));
#4925=CARTESIAN_POINT('',(-2.73963702891815,0.,5.));
#4926=CARTESIAN_POINT('',(-4.435,-8.38883057415937E-17,5.));
#4927=CARTESIAN_POINT('Origin',(-3.75,0.,5.));
#4928=CARTESIAN_POINT('Origin',(-4.25518148554092,-0.875,5.));
#4929=CARTESIAN_POINT('',(-3.24481851445908,-0.875,5.5));
#4930=CARTESIAN_POINT('',(-3.24481851445908,-0.875,5.));
#4931=CARTESIAN_POINT('',(-4.25518148554092,-0.875,5.5));
#4932=CARTESIAN_POINT('',(-4.25518148554092,-0.875,5.5));
#4933=CARTESIAN_POINT('',(-4.25518148554092,-0.875,5.));
#4934=CARTESIAN_POINT('Origin',(-4.76036297108184,1.23733777851239E-16,
5.));
#4935=CARTESIAN_POINT('',(-4.76036297108184,1.11022302462516E-16,5.5));
#4936=CARTESIAN_POINT('',(-4.76036297108184,1.23733777851239E-16,5.5));
#4937=CARTESIAN_POINT('',(-4.76036297108184,1.23733777851239E-16,5.));
#4938=CARTESIAN_POINT('Origin',(-4.25518148554092,0.875,5.));
#4939=CARTESIAN_POINT('',(-4.25518148554092,0.875,5.5));
#4940=CARTESIAN_POINT('',(-4.25518148554092,0.875,5.5));
#4941=CARTESIAN_POINT('',(-4.25518148554092,0.875,5.));
#4942=CARTESIAN_POINT('Origin',(-3.24481851445908,0.875,5.));
#4943=CARTESIAN_POINT('',(-3.24481851445908,0.875,5.5));
#4944=CARTESIAN_POINT('',(-3.24481851445908,0.875,5.5));
#4945=CARTESIAN_POINT('',(-3.24481851445908,0.875,5.));
#4946=CARTESIAN_POINT('Origin',(-2.73963702891815,0.,5.));
#4947=CARTESIAN_POINT('',(-2.73963702891815,0.,5.5));
#4948=CARTESIAN_POINT('',(-2.73963702891815,0.,5.5));
#4949=CARTESIAN_POINT('',(-2.73963702891815,0.,5.));
#4950=CARTESIAN_POINT('Origin',(-3.24481851445908,-0.875,5.));
#4951=CARTESIAN_POINT('',(-3.24481851445908,-0.875,5.5));
#4952=CARTESIAN_POINT('Origin',(-3.75,0.,5.5));
#4953=CARTESIAN_POINT('Origin',(-3.75,0.,3.8));
#4954=CARTESIAN_POINT('',(-3.95,-2.44929359829471E-17,3.8));
#4955=CARTESIAN_POINT('',(-3.95,-2.44929359829471E-17,3.8));
#4956=CARTESIAN_POINT('Origin',(-3.75,0.,3.8));
#4957=CARTESIAN_POINT('Origin',(-3.75,0.,3.8));
#4958=CARTESIAN_POINT('',(-4.435,-8.38883057415937E-17,3.8));
#4959=CARTESIAN_POINT('',(-4.435,-8.38883057415937E-17,3.8));
#4960=CARTESIAN_POINT('Origin',(-3.75,0.,3.8));
#4961=CARTESIAN_POINT('Origin',(-3.75,0.,3.8));
#5607=UNCERTAINTY_MEASURE_WITH_UNIT(LENGTH_MEASURE(0.001),#5639,
'DISTANCE_ACCURACY_VALUE',
'Maximum model space distance between geometric entities at asserted c
onnectivities');
#5621=UNCERTAINTY_MEASURE_WITH_UNIT(LENGTH_MEASURE(0.001),#5639,
'DISTANCE_ACCURACY_VALUE',
'Maximum model space distance between geometric entities at asserted c
onnectivities');
#5624=(
GEOMETRIC_REPRESENTATION_CONTEXT(3)
GLOBAL_UNCERTAINTY_ASSIGNED_CONTEXT((#5607))
GLOBAL_UNIT_ASSIGNED_CONTEXT((#5639,#5641,#5642))
REPRESENTATION_CONTEXT('','3D')
);
#5638=(
GEOMETRIC_REPRESENTATION_CONTEXT(3)
GLOBAL_UNCERTAINTY_ASSIGNED_CONTEXT((#5621))
GLOBAL_UNIT_ASSIGNED_CONTEXT((#5639,#5641,#5642))
REPRESENTATION_CONTEXT('','3D')
);
#5639=(
LENGTH_UNIT()
NAMED_UNIT(*)
SI_UNIT(.CENTI.,.METRE.)
);
#5641=(
NAMED_UNIT(*)
PLANE_ANGLE_UNIT()
SI_UNIT($,.RADIAN.)
);
#5642=(
NAMED_UNIT(*)
SI_UNIT($,.STERADIAN.)
SOLID_ANGLE_UNIT()
);
#5645=SHAPE_DEFINITION_REPRESENTATION(#5661,#5702);
#5661=PRODUCT_DEFINITION_SHAPE('',$,#5719);
#5702=SHAPE_REPRESENTATION('',(#3396),#5624);
#5716=PRODUCT_DEFINITION_CONTEXT('part definition',#5766,'design');
#5719=PRODUCT_DEFINITION('1/4-1/8 in port reducer (3)',
'1/4-1/8 in port reducer (3)',#5735,#5716);
#5735=PRODUCT_DEFINITION_FORMATION('',$,#5770);
#5766=APPLICATION_CONTEXT(
'Core Data for Automotive Mechanical Design Process');
#5767=PRODUCT_CONTEXT('part definition',#5766,'mechanical');
#5770=PRODUCT('1/4-1/8 in port reducer (3)','1/4-1/8 in port reducer (3)',
'1/4-1/8 in port reducer (3)',(#5767));
#5847=COLOUR_RGB('Sky Blue',0.24,0.69,0.87);
#5848=FILL_AREA_STYLE_COLOUR('',#5847);
#5849=FILL_AREA_STYLE('',(#5848));
#5850=SURFACE_STYLE_FILL_AREA(#5849);
#5851=SURFACE_SIDE_STYLE('',(#5850));
#5852=SURFACE_STYLE_USAGE(.BOTH.,#5851);
#5853=PRESENTATION_STYLE_ASSIGNMENT((#5852));
ENDSEC;
END-ISO-10303-21;
